ISO-10303-21;
HEADER;
/* Generated by software containing ST-Developer
 * from STEP Tools, Inc. (www.steptools.com) 
 */

FILE_DESCRIPTION(
/* description */ ('Bin tilter linkage'),
/* implementation_level */ '2;1');

FILE_NAME(
/* name */ 'Pivot spacer 5 mm (3).step',
/* time_stamp */ '2026-10-28T03:26:24-07:00',
/* author */ (''),
/* organization */ (''),
/* preprocessor_version */ 'ST-DEVELOPER v20.2',
/* originating_system */ 'Autodesk Translation Framework v15.17.0.0',
/* authorisation */ '');

FILE_SCHEMA (('AUTOMOTIVE_DESIGN { 1 0 10303 214 3 1 1 }'));
ENDSEC;

DATA;
#10=MECHANICAL_DESIGN_GEOMETRIC_PRESENTATION_REPRESENTATION('',(#957),#23728);
#737=SHAPE_REPRESENTATION_RELATIONSHIP('SRR','None',#24205,#843);
#843=ADVANCED_BREP_SHAPE_REPRESENTATION('',(#1070),#23705);
#957=STYLED_ITEM('',(#24779),#1070);
#1070=MANIFOLD_SOLID_BREP('Body1',#12488);
#1439=FACE_BOUND('',#3658,.T.);
#1440=FACE_BOUND('',#3660,.T.);
#1801=PLANE('',#15118);
#1802=PLANE('',#15119);
#2526=FACE_OUTER_BOUND('',#3655,.T.);
#2527=FACE_OUTER_BOUND('',#3656,.T.);
#2528=FACE_OUTER_BOUND('',#3657,.T.);
#2529=FACE_OUTER_BOUND('',#3659,.T.);
#3655=EDGE_LOOP('',(#10741,#10742,#10743,#10744));
#3656=EDGE_LOOP('',(#10745,#10746,#10747,#10748));
#3657=EDGE_LOOP('',(#10749));
#3658=EDGE_LOOP('',(#10750));
#3659=EDGE_LOOP('',(#10751));
#3660=EDGE_LOOP('',(#10752));
#4364=LINE('',#22804,#5039);
#4365=LINE('',#22810,#5040);
#5039=VECTOR('',#18865,0.605);
#5040=VECTOR('',#18872,0.800000000000001);
#5854=CIRCLE('',#15113,0.605);
#5855=CIRCLE('',#15114,0.605);
#5856=CIRCLE('',#15116,0.800000000000001);
#5857=CIRCLE('',#15117,0.800000000000001);
#6753=VERTEX_POINT('',#22801);
#6754=VERTEX_POINT('',#22803);
#6755=VERTEX_POINT('',#22807);
#6756=VERTEX_POINT('',#22809);
#8110=EDGE_CURVE('',#6753,#6753,#5854,.T.);
#8111=EDGE_CURVE('',#6753,#6754,#4364,.T.);
#8112=EDGE_CURVE('',#6754,#6754,#5855,.T.);
#8113=EDGE_CURVE('',#6755,#6755,#5856,.T.);
#8114=EDGE_CURVE('',#6755,#6756,#4365,.T.);
#8115=EDGE_CURVE('',#6756,#6756,#5857,.T.);
#10741=ORIENTED_EDGE('',*,*,#8110,.F.);
#10742=ORIENTED_EDGE('',*,*,#8111,.T.);
#10743=ORIENTED_EDGE('',*,*,#8112,.T.);
#10744=ORIENTED_EDGE('',*,*,#8111,.F.);
#10745=ORIENTED_EDGE('',*,*,#8113,.F.);
#10746=ORIENTED_EDGE('',*,*,#8114,.T.);
#10747=ORIENTED_EDGE('',*,*,#8115,.T.);
#10748=ORIENTED_EDGE('',*,*,#8114,.F.);
#10749=ORIENTED_EDGE('',*,*,#8113,.T.);
#10750=ORIENTED_EDGE('',*,*,#8110,.T.);
#10751=ORIENTED_EDGE('',*,*,#8115,.F.);
#10752=ORIENTED_EDGE('',*,*,#8112,.F.);
#11570=CYLINDRICAL_SURFACE('',#15112,0.605);
#11571=CYLINDRICAL_SURFACE('',#15115,0.800000000000001);
#12251=ADVANCED_FACE('',(#2526),#11570,.F.);
#12252=ADVANCED_FACE('',(#2527),#11571,.T.);
#12253=ADVANCED_FACE('',(#2528,#1439),#1801,.T.);
#12254=ADVANCED_FACE('',(#2529,#1440),#1802,.F.);
#12488=CLOSED_SHELL('',(#12251,#12252,#12253,#12254));
#15111=AXIS2_PLACEMENT_3D('',#22799,#18859,#18860);
#15112=AXIS2_PLACEMENT_3D('',#22800,#18861,#18862);
#15113=AXIS2_PLACEMENT_3D('',#22802,#18863,#18864);
#15114=AXIS2_PLACEMENT_3D('',#22805,#18866,#18867);
#15115=AXIS2_PLACEMENT_3D('',#22806,#18868,#18869);
#15116=AXIS2_PLACEMENT_3D('',#22808,#18870,#18871);
#15117=AXIS2_PLACEMENT_3D('',#22811,#18873,#18874);
#15118=AXIS2_PLACEMENT_3D('',#22812,#18875,#18876);
#15119=AXIS2_PLACEMENT_3D('',#22813,#18877,#18878);
#18859=DIRECTION('axis',(0.,0.,1.));
#18860=DIRECTION('refdir',(1.,0.,0.));
#18861=DIRECTION('center_axis',(0.,1.,0.));
#18862=DIRECTION('ref_axis',(1.,0.,0.));
#18863=DIRECTION('center_axis',(0.,-1.,0.));
#18864=DIRECTION('ref_axis',(1.,0.,0.));
#18865=DIRECTION('',(0.,-1.,0.));
#18866=DIRECTION('center_axis',(0.,-1.,0.));
#18867=DIRECTION('ref_axis',(1.,0.,0.));
#18868=DIRECTION('center_axis',(0.,1.,0.));
#18869=DIRECTION('ref_axis',(1.,0.,0.));
#18870=DIRECTION('center_axis',(0.,1.,0.));
#18871=DIRECTION('ref_axis',(1.,0.,0.));
#18872=DIRECTION('',(0.,-1.,0.));
#18873=DIRECTION('center_axis',(0.,1.,0.));
#18874=DIRECTION('ref_axis',(1.,0.,0.));
#18875=DIRECTION('center_axis',(0.,1.,0.));
#18876=DIRECTION('ref_axis',(1.,0.,0.));
#18877=DIRECTION('center_axis',(0.,1.,0.));
#18878=DIRECTION('ref_axis',(1.,0.,0.));
#22799=CARTESIAN_POINT('',(0.,0.,0.));
#22800=CARTESIAN_POINT('Origin',(24.2020784790221,-1.,28.6577532024872));
#22801=CARTESIAN_POINT('',(23.5970784790221,-0.5,28.6577532024872));
#22802=CARTESIAN_POINT('Origin',(24.2020784790221,-0.5,28.6577532024872));
#22803=CARTESIAN_POINT('',(23.5970784790221,-1.,28.6577532024872));
#22804=CARTESIAN_POINT('',(23.5970784790221,-1.,28.6577532024872));
#22805=CARTESIAN_POINT('Origin',(24.2020784790221,-1.,28.6577532024872));
#22806=CARTESIAN_POINT('Origin',(24.2020784790221,-1.,28.6577532024872));
#22807=CARTESIAN_POINT('',(23.4020784790221,-0.5,28.6577532024872));
#22808=CARTESIAN_POINT('Origin',(24.2020784790221,-0.5,28.6577532024872));
#22809=CARTESIAN_POINT('',(23.4020784790221,-1.,28.6577532024872));
#22810=CARTESIAN_POINT('',(23.4020784790221,-1.,28.6577532024872));
#22811=CARTESIAN_POINT('Origin',(24.2020784790221,-1.,28.6577532024872));
#22812=CARTESIAN_POINT('Origin',(24.2020784790221,-0.5,28.6577532024872));
#22813=CARTESIAN_POINT('Origin',(24.2020784790221,-1.,28.6577532024872));
#23588=UNCERTAINTY_MEASURE_WITH_UNIT(LENGTH_MEASURE(0.001),#23729,
'DISTANCE_ACCURACY_VALUE',
'Maximum model space distance between geometric entities at asserted c
onnectivities');
#23611=UNCERTAINTY_MEASURE_WITH_UNIT(LENGTH_MEASURE(0.001),#23729,
'DISTANCE_ACCURACY_VALUE',
'Maximum model space distance between geometric entities at asserted c
onnectivities');
#23705=(
GEOMETRIC_REPRESENTATION_CONTEXT(3)
GLOBAL_UNCERTAINTY_ASSIGNED_CONTEXT((#23588))
GLOBAL_UNIT_ASSIGNED_CONTEXT((#23729,#23731,#23732))
REPRESENTATION_CONTEXT('','3D')
);
#23728=(
GEOMETRIC_REPRESENTATION_CONTEXT(3)
GLOBAL_UNCERTAINTY_ASSIGNED_CONTEXT((#23611))
GLOBAL_UNIT_ASSIGNED_CONTEXT((#23729,#23731,#23732))
REPRESENTATION_CONTEXT('','3D')
);
#23729=(
LENGTH_UNIT()
NAMED_UNIT(*)
SI_UNIT(.CENTI.,.METRE.)
);
#23731=(
NAMED_UNIT(*)
PLANE_ANGLE_UNIT()
SI_UNIT($,.RADIAN.)
);
#23732=(
NAMED_UNIT(*)
SI_UNIT($,.STERADIAN.)
SOLID_ANGLE_UNIT()
);
#23826=SHAPE_DEFINITION_REPRESENTATION(#23993,#24205);
#23993=PRODUCT_DEFINITION_SHAPE('',$,#24322);
#24205=SHAPE_REPRESENTATION('',(#15111),#23705);
#24228=PRODUCT_DEFINITION_CONTEXT('part definition',#24578,'design');
#24322=PRODUCT_DEFINITION('Pivot spacer 5 mm (3)','Pivot spacer 5 mm (3)',
#24438,#24228);
#24438=PRODUCT_DEFINITION_FORMATION('',$,#24673);
#24578=APPLICATION_CONTEXT(
'Core Data for Automotive Mechanical Design Process');
#24579=PRODUCT_CONTEXT('part definition',#24578,'mechanical');
#24673=PRODUCT('Pivot spacer 5 mm (3)','Pivot spacer 5 mm (3)',
'Pivot spacer 5 mm (3)',(#24579));
#24773=COLOUR_RGB('Off White',0.89,0.88,0.83);
#24774=FILL_AREA_STYLE_COLOUR('',#24773);
#24775=FILL_AREA_STYLE('',(#24774));
#24776=SURFACE_STYLE_FILL_AREA(#24775);
#24777=SURFACE_SIDE_STYLE('',(#24776));
#24778=SURFACE_STYLE_USAGE(.BOTH.,#24777);
#24779=PRESENTATION_STYLE_ASSIGNMENT((#24778));
ENDSEC;
END-ISO-10303-21;
